ISO-10303-21;
HEADER;
/* Generated by software containing ST-Developer
 * from STEP Tools, Inc. (www.steptools.com) 
 */

FILE_DESCRIPTION(
/* description */ ('Double-row support with tensioned shaft'),
/* implementation_level */ '2;1');

FILE_NAME(
/* name */ 'Bonded foot pad (1).step',
/* time_stamp */ '2026-10-27T10:50:35-07:00',
/* author */ (''),
/* organization */ (''),
/* preprocessor_version */ 'ST-DEVELOPER v20.2',
/* originating_system */ 'Autodesk Translation Framework v15.17.0.0',
/* authorisation */ '');

FILE_SCHEMA (('AUTOMOTIVE_DESIGN { 1 0 10303 214 3 1 1 }'));
ENDSEC;

DATA;
#10=MECHANICAL_DESIGN_GEOMETRIC_PRESENTATION_REPRESENTATION('',(#481),#11559);
#417=SHAPE_REPRESENTATION_RELATIONSHIP('SRR','None',#11725,#449);
#449=ADVANCED_BREP_SHAPE_REPRESENTATION('',(#514),#11527);
#481=STYLED_ITEM('',(#11960),#514);
#514=MANIFOLD_SOLID_BREP('Body1',#6326);
#691=PLANE('',#6766);
#692=PLANE('',#6767);
#693=PLANE('',#6768);
#694=PLANE('',#6769);
#695=PLANE('',#6770);
#696=PLANE('',#6771);
#941=FACE_OUTER_BOUND('',#1309,.T.);
#942=FACE_OUTER_BOUND('',#1310,.T.);
#943=FACE_OUTER_BOUND('',#1311,.T.);
#944=FACE_OUTER_BOUND('',#1312,.T.);
#945=FACE_OUTER_BOUND('',#1313,.T.);
#946=FACE_OUTER_BOUND('',#1314,.T.);
#1309=EDGE_LOOP('',(#4450,#4451,#4452,#4453));
#1310=EDGE_LOOP('',(#4454,#4455,#4456,#4457));
#1311=EDGE_LOOP('',(#4458,#4459,#4460,#4461));
#1312=EDGE_LOOP('',(#4462,#4463,#4464,#4465));
#1313=EDGE_LOOP('',(#4466,#4467,#4468,#4469));
#1314=EDGE_LOOP('',(#4470,#4471,#4472,#4473));
#1778=LINE('',#9366,#2325);
#1779=LINE('',#9368,#2326);
#1780=LINE('',#9370,#2327);
#1781=LINE('',#9371,#2328);
#1782=LINE('',#9374,#2329);
#1783=LINE('',#9376,#2330);
#1784=LINE('',#9377,#2331);
#1785=LINE('',#9380,#2332);
#1786=LINE('',#9382,#2333);
#1787=LINE('',#9383,#2334);
#1788=LINE('',#9385,#2335);
#1789=LINE('',#9386,#2336);
#2325=VECTOR('',#7515,1.);
#2326=VECTOR('',#7516,1.);
#2327=VECTOR('',#7517,1.);
#2328=VECTOR('',#7518,1.);
#2329=VECTOR('',#7521,1.);
#2330=VECTOR('',#7522,1.);
#2331=VECTOR('',#7523,1.);
#2332=VECTOR('',#7526,1.);
#2333=VECTOR('',#7527,1.);
#2334=VECTOR('',#7528,1.);
#2335=VECTOR('',#7531,1.);
#2336=VECTOR('',#7532,1.);
#3067=VERTEX_POINT('',#9364);
#3068=VERTEX_POINT('',#9365);
#3069=VERTEX_POINT('',#9367);
#3070=VERTEX_POINT('',#9369);
#3071=VERTEX_POINT('',#9373);
#3072=VERTEX_POINT('',#9375);
#3073=VERTEX_POINT('',#9379);
#3074=VERTEX_POINT('',#9381);
#3610=EDGE_CURVE('',#3067,#3068,#1778,.T.);
#3611=EDGE_CURVE('',#3068,#3069,#1779,.T.);
#3612=EDGE_CURVE('',#3070,#3069,#1780,.T.);
#3613=EDGE_CURVE('',#3067,#3070,#1781,.T.);
#3614=EDGE_CURVE('',#3071,#3067,#1782,.T.);
#3615=EDGE_CURVE('',#3072,#3070,#1783,.T.);
#3616=EDGE_CURVE('',#3071,#3072,#1784,.T.);
#3617=EDGE_CURVE('',#3073,#3071,#1785,.T.);
#3618=EDGE_CURVE('',#3074,#3072,#1786,.T.);
#3619=EDGE_CURVE('',#3073,#3074,#1787,.T.);
#3620=EDGE_CURVE('',#3068,#3073,#1788,.T.);
#3621=EDGE_CURVE('',#3069,#3074,#1789,.T.);
#4450=ORIENTED_EDGE('',*,*,#3610,.T.);
#4451=ORIENTED_EDGE('',*,*,#3611,.T.);
#4452=ORIENTED_EDGE('',*,*,#3612,.F.);
#4453=ORIENTED_EDGE('',*,*,#3613,.F.);
#4454=ORIENTED_EDGE('',*,*,#3614,.T.);
#4455=ORIENTED_EDGE('',*,*,#3613,.T.);
#4456=ORIENTED_EDGE('',*,*,#3615,.F.);
#4457=ORIENTED_EDGE('',*,*,#3616,.F.);
#4458=ORIENTED_EDGE('',*,*,#3617,.T.);
#4459=ORIENTED_EDGE('',*,*,#3616,.T.);
#4460=ORIENTED_EDGE('',*,*,#3618,.F.);
#4461=ORIENTED_EDGE('',*,*,#3619,.F.);
#4462=ORIENTED_EDGE('',*,*,#3620,.T.);
#4463=ORIENTED_EDGE('',*,*,#3619,.T.);
#4464=ORIENTED_EDGE('',*,*,#3621,.F.);
#4465=ORIENTED_EDGE('',*,*,#3611,.F.);
#4466=ORIENTED_EDGE('',*,*,#3621,.T.);
#4467=ORIENTED_EDGE('',*,*,#3618,.T.);
#4468=ORIENTED_EDGE('',*,*,#3615,.T.);
#4469=ORIENTED_EDGE('',*,*,#3612,.T.);
#4470=ORIENTED_EDGE('',*,*,#3620,.F.);
#4471=ORIENTED_EDGE('',*,*,#3610,.F.);
#4472=ORIENTED_EDGE('',*,*,#3614,.F.);
#4473=ORIENTED_EDGE('',*,*,#3617,.F.);
#6004=ADVANCED_FACE('',(#941),#691,.T.);
#6005=ADVANCED_FACE('',(#942),#692,.T.);
#6006=ADVANCED_FACE('',(#943),#693,.T.);
#6007=ADVANCED_FACE('',(#944),#694,.T.);
#6008=ADVANCED_FACE('',(#945),#695,.T.);
#6009=ADVANCED_FACE('',(#946),#696,.F.);
#6326=CLOSED_SHELL('',(#6004,#6005,#6006,#6007,#6008,#6009));
#6765=AXIS2_PLACEMENT_3D('',#9362,#7511,#7512);
#6766=AXIS2_PLACEMENT_3D('',#9363,#7513,#7514);
#6767=AXIS2_PLACEMENT_3D('',#9372,#7519,#7520);
#6768=AXIS2_PLACEMENT_3D('',#9378,#7524,#7525);
#6769=AXIS2_PLACEMENT_3D('',#9384,#7529,#7530);
#6770=AXIS2_PLACEMENT_3D('',#9387,#7533,#7534);
#6771=AXIS2_PLACEMENT_3D('',#9388,#7535,#7536);
#7511=DIRECTION('axis',(0.,0.,1.));
#7512=DIRECTION('refdir',(1.,0.,0.));
#7513=DIRECTION('center_axis',(0.,1.,0.));
#7514=DIRECTION('ref_axis',(-1.,0.,0.));
#7515=DIRECTION('',(-1.,0.,0.));
#7516=DIRECTION('',(0.,0.,1.));
#7517=DIRECTION('',(-1.,0.,0.));
#7518=DIRECTION('',(0.,0.,1.));
#7519=DIRECTION('center_axis',(1.,0.,0.));
#7520=DIRECTION('ref_axis',(0.,1.,0.));
#7521=DIRECTION('',(0.,1.,0.));
#7522=DIRECTION('',(0.,1.,0.));
#7523=DIRECTION('',(0.,0.,1.));
#7524=DIRECTION('center_axis',(0.,-1.,0.));
#7525=DIRECTION('ref_axis',(1.,0.,0.));
#7526=DIRECTION('',(1.,0.,0.));
#7527=DIRECTION('',(1.,0.,0.));
#7528=DIRECTION('',(0.,0.,1.));
#7529=DIRECTION('center_axis',(-1.,0.,0.));
#7530=DIRECTION('ref_axis',(0.,-1.,0.));
#7531=DIRECTION('',(0.,-1.,0.));
#7532=DIRECTION('',(0.,-1.,0.));
#7533=DIRECTION('center_axis',(0.,0.,1.));
#7534=DIRECTION('ref_axis',(1.,0.,0.));
#7535=DIRECTION('center_axis',(0.,0.,1.));
#7536=DIRECTION('ref_axis',(1.,0.,0.));
#9362=CARTESIAN_POINT('',(0.,0.,0.));
#9363=CARTESIAN_POINT('Origin',(10.,6.,-0.4));
#9364=CARTESIAN_POINT('',(10.,6.,-0.4));
#9365=CARTESIAN_POINT('',(-10.,6.,-0.4));
#9366=CARTESIAN_POINT('',(10.,6.,-0.4));
#9367=CARTESIAN_POINT('',(-10.,6.,0.));
#9368=CARTESIAN_POINT('',(-10.,6.,-0.4));
#9369=CARTESIAN_POINT('',(10.,6.,0.));
#9370=CARTESIAN_POINT('',(10.,6.,0.));
#9371=CARTESIAN_POINT('',(10.,6.,-0.4));
#9372=CARTESIAN_POINT('Origin',(10.,4.,-0.4));
#9373=CARTESIAN_POINT('',(10.,4.,-0.4));
#9374=CARTESIAN_POINT('',(10.,4.,-0.4));
#9375=CARTESIAN_POINT('',(10.,4.,0.));
#9376=CARTESIAN_POINT('',(10.,4.,0.));
#9377=CARTESIAN_POINT('',(10.,4.,-0.4));
#9378=CARTESIAN_POINT('Origin',(-10.,4.,-0.4));
#9379=CARTESIAN_POINT('',(-10.,4.,-0.4));
#9380=CARTESIAN_POINT('',(-10.,4.,-0.4));
#9381=CARTESIAN_POINT('',(-10.,4.,0.));
#9382=CARTESIAN_POINT('',(-10.,4.,0.));
#9383=CARTESIAN_POINT('',(-10.,4.,-0.4));
#9384=CARTESIAN_POINT('Origin',(-10.,6.,-0.4));
#9385=CARTESIAN_POINT('',(-10.,6.,-0.4));
#9386=CARTESIAN_POINT('',(-10.,6.,0.));
#9387=CARTESIAN_POINT('Origin',(0.,5.,0.));
#9388=CARTESIAN_POINT('Origin',(0.,5.,-0.4));
#11490=UNCERTAINTY_MEASURE_WITH_UNIT(LENGTH_MEASURE(0.001),#11560,
'DISTANCE_ACCURACY_VALUE',
'Maximum model space distance between geometric entities at asserted c
onnectivities');
#11522=UNCERTAINTY_MEASURE_WITH_UNIT(LENGTH_MEASURE(0.001),#11560,
'DISTANCE_ACCURACY_VALUE',
'Maximum model space distance between geometric entities at asserted c
onnectivities');
#11527=(
GEOMETRIC_REPRESENTATION_CONTEXT(3)
GLOBAL_UNCERTAINTY_ASSIGNED_CONTEXT((#11490))
GLOBAL_UNIT_ASSIGNED_CONTEXT((#11560,#11562,#11563))
REPRESENTATION_CONTEXT('','3D')
);
#11559=(
GEOMETRIC_REPRESENTATION_CONTEXT(3)
GLOBAL_UNCERTAINTY_ASSIGNED_CONTEXT((#11522))
GLOBAL_UNIT_ASSIGNED_CONTEXT((#11560,#11562,#11563))
REPRESENTATION_CONTEXT('','3D')
);
#11560=(
LENGTH_UNIT()
NAMED_UNIT(*)
SI_UNIT(.CENTI.,.METRE.)
);
#11562=(
NAMED_UNIT(*)
PLANE_ANGLE_UNIT()
SI_UNIT($,.RADIAN.)
);
#11563=(
NAMED_UNIT(*)
SI_UNIT($,.STERADIAN.)
SOLID_ANGLE_UNIT()
);
#11568=SHAPE_DEFINITION_REPRESENTATION(#11604,#11725);
#11604=PRODUCT_DEFINITION_SHAPE('',$,#11762);
#11725=SHAPE_REPRESENTATION('',(#6765),#11527);
#11757=PRODUCT_DEFINITION_CONTEXT('part definition',#11867,'design');
#11762=PRODUCT_DEFINITION('Bonded foot pad (1)','Bonded foot pad (1)',#11798,
#11757);
#11798=PRODUCT_DEFINITION_FORMATION('',$,#11873);
#11867=APPLICATION_CONTEXT(
'Core Data for Automotive Mechanical Design Process');
#11868=PRODUCT_CONTEXT('part definition',#11867,'mechanical');
#11873=PRODUCT('Bonded foot pad (1)','Bonded foot pad (1)',
'Bonded foot pad (1)',(#11868));
#11954=COLOUR_RGB('Sky Blue',0.24,0.69,0.87);
#11955=FILL_AREA_STYLE_COLOUR('',#11954);
#11956=FILL_AREA_STYLE('',(#11955));
#11957=SURFACE_STYLE_FILL_AREA(#11956);
#11958=SURFACE_SIDE_STYLE('',(#11957));
#11959=SURFACE_STYLE_USAGE(.BOTH.,#11958);
#11960=PRESENTATION_STYLE_ASSIGNMENT((#11959));
ENDSEC;
END-ISO-10303-21;
